ISO-10303-21;
HEADER;
/* Generated by software containing ST-Developer
 * from STEP Tools, Inc. (www.steptools.com) 
 */

FILE_DESCRIPTION(
/* description */ ('Crank-driven oscillating fan base (mechanism only)'),

/* implementation_level */ '2;1');

FILE_NAME(
/* name */ 'Front link spacer (1).step',
/* time_stamp */ '2026-10-28T03:25:00-07:00',
/* author */ (''),
/* organization */ (''),
/* preprocessor_version */ 'ST-DEVELOPER v20.2',
/* originating_system */ 'Autodesk Translation Framework v15.17.0.0',
/* authorisation */ '');

FILE_SCHEMA (('AUTOMOTIVE_DESIGN { 1 0 10303 214 3 1 1 }'));
ENDSEC;

DATA;
#10=MECHANICAL_DESIGN_GEOMETRIC_PRESENTATION_REPRESENTATION('',(#476),#11916);
#388=SHAPE_REPRESENTATION_RELATIONSHIP('SRR','None',#12115,#428);
#428=ADVANCED_BREP_SHAPE_REPRESENTATION('',(#523),#11906);
#476=STYLED_ITEM('',(#12361),#523);
#523=MANIFOLD_SOLID_BREP('Body1',#6107);
#675=FACE_BOUND('',#1712,.T.);
#676=FACE_BOUND('',#1714,.T.);
#841=PLANE('',#7229);
#842=PLANE('',#7230);
#1189=FACE_OUTER_BOUND('',#1709,.T.);
#1190=FACE_OUTER_BOUND('',#1710,.T.);
#1191=FACE_OUTER_BOUND('',#1711,.T.);
#1192=FACE_OUTER_BOUND('',#1713,.T.);
#1709=EDGE_LOOP('',(#5280,#5281,#5282,#5283));
#1710=EDGE_LOOP('',(#5284,#5285,#5286,#5287));
#1711=EDGE_LOOP('',(#5288));
#1712=EDGE_LOOP('',(#5289));
#1713=EDGE_LOOP('',(#5290));
#1714=EDGE_LOOP('',(#5291));
#2044=LINE('',#11466,#2377);
#2045=LINE('',#11472,#2378);
#2377=VECTOR('',#8989,0.305);
#2378=VECTOR('',#8996,0.5);
#2783=CIRCLE('',#7224,0.305);
#2784=CIRCLE('',#7225,0.305);
#2785=CIRCLE('',#7227,0.5);
#2786=CIRCLE('',#7228,0.5);
#3243=VERTEX_POINT('',#11463);
#3244=VERTEX_POINT('',#11465);
#3245=VERTEX_POINT('',#11469);
#3246=VERTEX_POINT('',#11471);
#3935=EDGE_CURVE('',#3243,#3243,#2783,.T.);
#3936=EDGE_CURVE('',#3243,#3244,#2044,.T.);
#3937=EDGE_CURVE('',#3244,#3244,#2784,.T.);
#3938=EDGE_CURVE('',#3245,#3245,#2785,.T.);
#3939=EDGE_CURVE('',#3245,#3246,#2045,.T.);
#3940=EDGE_CURVE('',#3246,#3246,#2786,.T.);
#5280=ORIENTED_EDGE('',*,*,#3935,.F.);
#5281=ORIENTED_EDGE('',*,*,#3936,.T.);
#5282=ORIENTED_EDGE('',*,*,#3937,.T.);
#5283=ORIENTED_EDGE('',*,*,#3936,.F.);
#5284=ORIENTED_EDGE('',*,*,#3938,.F.);
#5285=ORIENTED_EDGE('',*,*,#3939,.T.);
#5286=ORIENTED_EDGE('',*,*,#3940,.T.);
#5287=ORIENTED_EDGE('',*,*,#3939,.F.);
#5288=ORIENTED_EDGE('',*,*,#3938,.T.);
#5289=ORIENTED_EDGE('',*,*,#3935,.T.);
#5290=ORIENTED_EDGE('',*,*,#3940,.F.);
#5291=ORIENTED_EDGE('',*,*,#3937,.F.);
#5673=CYLINDRICAL_SURFACE('',#7223,0.305);
#5674=CYLINDRICAL_SURFACE('',#7226,0.5);
#5995=ADVANCED_FACE('',(#1189),#5673,.F.);
#5996=ADVANCED_FACE('',(#1190),#5674,.T.);
#5997=ADVANCED_FACE('',(#1191,#675),#841,.T.);
#5998=ADVANCED_FACE('',(#1192,#676),#842,.F.);
#6107=CLOSED_SHELL('',(#5995,#5996,#5997,#5998));
#7222=AXIS2_PLACEMENT_3D('',#11461,#8983,#8984);
#7223=AXIS2_PLACEMENT_3D('',#11462,#8985,#8986);
#7224=AXIS2_PLACEMENT_3D('',#11464,#8987,#8988);
#7225=AXIS2_PLACEMENT_3D('',#11467,#8990,#8991);
#7226=AXIS2_PLACEMENT_3D('',#11468,#8992,#8993);
#7227=AXIS2_PLACEMENT_3D('',#11470,#8994,#8995);
#7228=AXIS2_PLACEMENT_3D('',#11473,#8997,#8998);
#7229=AXIS2_PLACEMENT_3D('',#11474,#8999,#9000);
#7230=AXIS2_PLACEMENT_3D('',#11475,#9001,#9002);
#8983=DIRECTION('axis',(0.,0.,1.));
#8984=DIRECTION('refdir',(1.,0.,0.));
#8985=DIRECTION('center_axis',(0.,0.,1.));
#8986=DIRECTION('ref_axis',(1.,0.,0.));
#8987=DIRECTION('center_axis',(0.,0.,-1.));
#8988=DIRECTION('ref_axis',(1.,0.,0.));
#8989=DIRECTION('',(0.,0.,-1.));
#8990=DIRECTION('center_axis',(0.,0.,-1.));
#8991=DIRECTION('ref_axis',(1.,0.,0.));
#8992=DIRECTION('center_axis',(0.,0.,1.));
#8993=DIRECTION('ref_axis',(1.,0.,0.));
#8994=DIRECTION('center_axis',(0.,0.,1.));
#8995=DIRECTION('ref_axis',(1.,0.,0.));
#8996=DIRECTION('',(0.,0.,-1.));
#8997=DIRECTION('center_axis',(0.,0.,1.));
#8998=DIRECTION('ref_axis',(1.,0.,0.));
#8999=DIRECTION('center_axis',(0.,0.,1.));
#9000=DIRECTION('ref_axis',(1.,0.,0.));
#9001=DIRECTION('center_axis',(0.,0.,1.));
#9002=DIRECTION('ref_axis',(1.,0.,0.));
#11461=CARTESIAN_POINT('',(0.,0.,0.));
#11462=CARTESIAN_POINT('Origin',(8.,4.,9.4));
#11463=CARTESIAN_POINT('',(7.695,4.,9.6));
#11464=CARTESIAN_POINT('Origin',(8.,4.,9.6));
#11465=CARTESIAN_POINT('',(7.695,4.,9.4));
#11466=CARTESIAN_POINT('',(7.695,4.,9.4));
#11467=CARTESIAN_POINT('Origin',(8.,4.,9.4));
#11468=CARTESIAN_POINT('Origin',(8.,4.,9.4));
#11469=CARTESIAN_POINT('',(7.5,4.,9.6));
#11470=CARTESIAN_POINT('Origin',(8.,4.,9.6));
#11471=CARTESIAN_POINT('',(7.5,4.,9.4));
#11472=CARTESIAN_POINT('',(7.5,4.,9.4));
#11473=CARTESIAN_POINT('Origin',(8.,4.,9.4));
#11474=CARTESIAN_POINT('Origin',(8.,4.,9.6));
#11475=CARTESIAN_POINT('Origin',(8.,4.,9.4));
#11859=UNCERTAINTY_MEASURE_WITH_UNIT(LENGTH_MEASURE(0.001),#11917,
'DISTANCE_ACCURACY_VALUE',
'Maximum model space distance between geometric entities at asserted c
onnectivities');
#11869=UNCERTAINTY_MEASURE_WITH_UNIT(LENGTH_MEASURE(0.001),#11917,
'DISTANCE_ACCURACY_VALUE',
'Maximum model space distance between geometric entities at asserted c
onnectivities');
#11906=(
GEOMETRIC_REPRESENTATION_CONTEXT(3)
GLOBAL_UNCERTAINTY_ASSIGNED_CONTEXT((#11859))
GLOBAL_UNIT_ASSIGNED_CONTEXT((#11917,#11919,#11920))
REPRESENTATION_CONTEXT('','3D')
);
#11916=(
GEOMETRIC_REPRESENTATION_CONTEXT(3)
GLOBAL_UNCERTAINTY_ASSIGNED_CONTEXT((#11869))
GLOBAL_UNIT_ASSIGNED_CONTEXT((#11917,#11919,#11920))
REPRESENTATION_CONTEXT('','3D')
);
#11917=(
LENGTH_UNIT()
NAMED_UNIT(*)
SI_UNIT(.CENTI.,.METRE.)
);
#11919=(
NAMED_UNIT(*)
PLANE_ANGLE_UNIT()
SI_UNIT($,.RADIAN.)
);
#11920=(
NAMED_UNIT(*)
SI_UNIT($,.STERADIAN.)
SOLID_ANGLE_UNIT()
);
#11957=SHAPE_DEFINITION_REPRESENTATION(#12008,#12115);
#12008=PRODUCT_DEFINITION_SHAPE('',$,#12162);
#12115=SHAPE_REPRESENTATION('',(#7222),#11906);
#12125=PRODUCT_DEFINITION_CONTEXT('part definition',#12265,'design');
#12162=PRODUCT_DEFINITION('Front link spacer (1)','Front link spacer (1)',
#12208,#12125);
#12208=PRODUCT_DEFINITION_FORMATION('',$,#12303);
#12265=APPLICATION_CONTEXT(
'Core Data for Automotive Mechanical Design Process');
#12266=PRODUCT_CONTEXT('part definition',#12265,'mechanical');
#12303=PRODUCT('Front link spacer (1)','Front link spacer (1)',
'Front link spacer (1)',(#12266));
#12355=COLOUR_RGB('Light Blue',0.38,0.62,0.78);
#12356=FILL_AREA_STYLE_COLOUR('',#12355);
#12357=FILL_AREA_STYLE('',(#12356));
#12358=SURFACE_STYLE_FILL_AREA(#12357);
#12359=SURFACE_SIDE_STYLE('',(#12358));
#12360=SURFACE_STYLE_USAGE(.BOTH.,#12359);
#12361=PRESENTATION_STYLE_ASSIGNMENT((#12360));
ENDSEC;
END-ISO-10303-21;
